ISO-10303-21;
HEADER;
FILE_DESCRIPTION (('STEP AP214'),
    '1' );
FILE_NAME ('Oil seal.step',
    '2026-10-22T18:53:08',
    ( '' ),
    ( '' ),
    'SwSTEP 2.0',
    'SolidWorks 2025',
    '' );
FILE_SCHEMA (( 'AUTOMOTIVE_DESIGN' ));
ENDSEC;

DATA;
#8=FACE_OUTER_BOUND ( 'NONE', #14031, .T. ) ;
#29=ORIENTED_EDGE ( 'NONE', *, *, #14693, .F. ) ;
#44=ORIENTED_EDGE ( 'NONE', *, *, #15427, .T. ) ;
#61=VECTOR ( 'NONE', #8595, 1000.000000000000000 ) ;
#76=TOROIDAL_SURFACE ( 'NONE', #15632, 14.42592346043842433, 0.2999999999999999334 ) ;
#83=EDGE_LOOP ( 'NONE', ( #14204, #20544 ) ) ;
#94=CARTESIAN_POINT ( 'NONE',  ( 3.530011532367169913, 0.000000000000000000, 11.23654394515110511 ) ) ;
#99=FACE_OUTER_BOUND ( 'NONE', #13945, .T. ) ;
#179=DIRECTION ( 'NONE',  ( 0.000000000000000000, 0.000000000000000000, 1.000000000000000000 ) ) ;
#270=DIRECTION ( 'NONE',  ( 0.000000000000000000, 0.000000000000000000, 1.000000000000000000 ) ) ;
#314=EDGE_LOOP ( 'NONE', ( #13225, #21297, #22979, #6998 ) ) ;
#367=DIRECTION ( 'NONE',  ( 0.000000000000000000, 0.000000000000000000, 1.000000000000000000 ) ) ;
#371=CARTESIAN_POINT ( 'NONE',  ( 0.2999999999999999889, 1.227821507548370807E-15, -10.02592346138681023 ) ) ;
#379=VERTEX_POINT ( 'NONE', #12752 ) ;
#408=ORIENTED_EDGE ( 'NONE', *, *, #12855, .T. ) ;
#441=ORIENTED_EDGE ( 'NONE', *, *, #3295, .T. ) ;
#483=DIRECTION ( 'NONE',  ( -1.000000000000000000, -0.000000000000000000, -0.000000000000000000 ) ) ;
#514=EDGE_LOOP ( 'NONE', ( #9069, #10444 ) ) ;
#518=AXIS2_PLACEMENT_3D ( 'NONE', #12701, #20041, #20167 ) ;
#551=ORIENTED_EDGE ( 'NONE', *, *, #872, .T. ) ;
#556=VERTEX_POINT ( 'NONE', #8143 ) ;
#595=CARTESIAN_POINT ( 'NONE',  ( 2.879195777975148768E-17, 1.227821507548370807E-15, -10.02592346138681023 ) ) ;
#681=EDGE_CURVE ( 'NONE', #2976, #15778, #14122, .T. ) ;
#702=VERTEX_POINT ( 'NONE', #22859 ) ;
#728=DIRECTION ( 'NONE',  ( 0.000000000000000000, -1.224646799147352221E-16, 1.000000000000000000 ) ) ;
#742=CARTESIAN_POINT ( 'NONE',  ( 0.9999999999999986677, 1.374779123446053458E-15, -11.22592346138681130 ) ) ;
#762=EDGE_CURVE ( 'NONE', #15778, #2103, #13814, .T. ) ;
#774=DIRECTION ( 'NONE',  ( -1.000000000000000000, -0.000000000000000000, -0.000000000000000000 ) ) ;
#811=CARTESIAN_POINT ( 'NONE',  ( 4.489900896931573904, 0.000000000000000000, 0.000000000000000000 ) ) ;
#852=SHAPE_REPRESENTATION ( 'Oil seal', ( #8005 ), #1445 ) ;
#872=EDGE_CURVE ( 'NONE', #15778, #2976, #11765, .T. ) ;
#881=CIRCLE ( 'NONE', #14887, 13.72592346138681130 ) ;
#906=AXIS2_PLACEMENT_3D ( 'NONE', #13168, #22574, #13282 ) ;
#908=CARTESIAN_POINT ( 'NONE',  ( 0.000000000000000000, 1.377380391735521048E-15, -11.24716442891539714 ) ) ;
#917=AXIS2_PLACEMENT_3D ( 'NONE', #94, #16678, #11144 ) ;
#984=EDGE_CURVE ( 'NONE', #18951, #10181, #23934, .T. ) ;
#1003=EDGE_LOOP ( 'NONE', ( #7605, #44, #18685, #22956 ) ) ;
#1016=DIRECTION ( 'NONE',  ( -1.000000000000000000, -0.000000000000000000, -0.000000000000000000 ) ) ;
#1024=AXIS2_PLACEMENT_3D ( 'NONE', #17998, #1293, #4604 ) ;
#1025=EDGE_CURVE ( 'NONE', #23079, #8542, #15656, .T. ) ;
#1062=PLANE ( 'NONE',  #12306 ) ;
#1069=DIRECTION ( 'NONE',  ( 0.000000000000000000, 0.000000000000000000, 1.000000000000000000 ) ) ;
#1087=UNCERTAINTY_MEASURE_WITH_UNIT (LENGTH_MEASURE( 1.000000000000000082E-05 ), #10598, 'distance_accuracy_value', 'NONE');
#1214=ORIENTED_EDGE ( 'NONE', *, *, #7886, .T. ) ;
#1245=DIRECTION ( 'NONE',  ( -1.000000000000000000, -0.000000000000000000, -0.000000000000000000 ) ) ;
#1261=CIRCLE ( 'NONE', #18405, 0.2999999999999999334 ) ;
#1268=CYLINDRICAL_SURFACE ( 'NONE', #6767, 11.24716442891539714 ) ;
#1284=DIRECTION ( 'NONE',  ( 0.000000000000000000, 0.000000000000000000, 1.000000000000000000 ) ) ;
#1285=DIRECTION ( 'NONE',  ( -1.000000000000000000, -0.000000000000000000, -0.000000000000000000 ) ) ;
#1293=DIRECTION ( 'NONE',  ( -1.000000000000000000, -0.000000000000000000, -0.000000000000000000 ) ) ;
#1395=CARTESIAN_POINT ( 'NONE',  ( 2.570122167802765922, 0.000000000000000000, 11.22592346138681130 ) ) ;
#1439=EDGE_LOOP ( 'NONE', ( #2545, #8145, #17255, #10137 ) ) ;
#1445=( GEOMETRIC_REPRESENTATION_CONTEXT ( 3 ) GLOBAL_UNCERTAINTY_ASSIGNED_CONTEXT ( ( #20850 ) ) GLOBAL_UNIT_ASSIGNED_CONTEXT ( ( #19253, #21330, #6565 ) ) REPRESENTATION_CONTEXT ( 'NONE', 'WORKASPACE' ) );
#1451=AXIS2_PLACEMENT_3D ( 'NONE', #5361, #5014, #1694 ) ;
#1503=DIRECTION ( 'NONE',  ( -1.000000000000000000, -0.000000000000000000, -0.000000000000000000 ) ) ;
#1610=ORIENTED_EDGE ( 'NONE', *, *, #17130, .F. ) ;
#1652=EDGE_LOOP ( 'NONE', ( #551, #12219, #17711, #13018 ) ) ;
#1670=DIRECTION ( 'NONE',  ( -1.000000000000000000, -0.000000000000000000, -0.000000000000000000 ) ) ;
#1694=DIRECTION ( 'NONE',  ( 0.000000000000000000, 0.000000000000000000, 1.000000000000000000 ) ) ;
#1716=ORIENTED_EDGE ( 'NONE', *, *, #21342, .F. ) ;
#1742=DIRECTION ( 'NONE',  ( -1.000000000000000000, -0.000000000000000000, -0.000000000000000000 ) ) ;
#1757=VECTOR ( 'NONE', #7727, 1000.000000000000000 ) ;
#1883=EDGE_CURVE ( 'NONE', #3309, #18733, #15902, .T. ) ;
#1993=VERTEX_POINT ( 'NONE', #1395 ) ;
#2037=CIRCLE ( 'NONE', #5161, 11.22592346138681130 ) ;
#2103=VERTEX_POINT ( 'NONE', #16722 ) ;
#2186=CARTESIAN_POINT ( 'NONE',  ( 5.078177448618336420, 1.340640987761100385E-15, -10.94716442891539643 ) ) ;
#2193=ORIENTED_EDGE ( 'NONE', *, *, #14693, .T. ) ;
#2255=VECTOR ( 'NONE', #3089, 1000.000000000000000 ) ;
#2345=VERTEX_POINT ( 'NONE', #7412 ) ;
#2428=ADVANCED_FACE ( 'NONE', ( #8 ), #3302, .T. ) ;
#2476=AXIS2_PLACEMENT_3D ( 'NONE', #17990, #3351, #6899 ) ;
#2545=ORIENTED_EDGE ( 'NONE', *, *, #15701, .T. ) ;
#2624=ORIENTED_EDGE ( 'NONE', *, *, #20392, .T. ) ;
#2663=EDGE_LOOP ( 'NONE', ( #19558, #24041, #23179, #12475 ) ) ;
#2706=ORIENTED_EDGE ( 'NONE', *, *, #16875, .F. ) ;
#2764=VERTEX_POINT ( 'NONE', #742 ) ;
#2771=AXIS2_PLACEMENT_3D ( 'NONE', #7752, #9456, #6067 ) ;
#2807=ORIENTED_EDGE ( 'NONE', *, *, #7972, .F. ) ;
#2818=EDGE_LOOP ( 'NONE', ( #11861, #3603 ) ) ;
#2839=DIRECTION ( 'NONE',  ( -1.000000000000000000, -0.000000000000000000, -0.000000000000000000 ) ) ;
#2873=DIRECTION ( 'NONE',  ( -1.000000000000000000, -0.000000000000000000, -0.000000000000000000 ) ) ;
#2900=ORIENTED_EDGE ( 'NONE', *, *, #4198, .F. ) ;
#2928=EDGE_LOOP ( 'NONE', ( #4590, #29 ) ) ;
#2957=DIRECTION ( 'NONE',  ( 0.000000000000000000, 0.000000000000000000, 1.000000000000000000 ) ) ;
#2961=DIRECTION ( 'NONE',  ( 0.000000000000000000, 0.000000000000000000, 1.000000000000000000 ) ) ;
#2976=VERTEX_POINT ( 'NONE', #14969 ) ;
#2980=AXIS2_PLACEMENT_3D ( 'NONE', #16196, #19976, #21698 ) ;
#3038=DIRECTION ( 'NONE',  ( 0.000000000000000000, 0.000000000000000000, 1.000000000000000000 ) ) ;
#3085=CARTESIAN_POINT ( 'NONE',  ( 0.000000000000000000, 0.000000000000000000, 0.000000000000000000 ) ) ;
#3089=DIRECTION ( 'NONE',  ( -1.000000000000000000, -0.000000000000000000, -0.000000000000000000 ) ) ;
#3113=CARTESIAN_POINT ( 'NONE',  ( 0.000000000000000000, 0.000000000000000000, 0.000000000000000000 ) ) ;
#3190=DIRECTION ( 'NONE',  ( 0.000000000000000000, 0.000000000000000000, 1.000000000000000000 ) ) ;
#3222=FACE_BOUND ( 'NONE', #15127, .T. ) ;
#3249=SHAPE_DEFINITION_REPRESENTATION ( #8643, #852 ) ;
#3295=EDGE_CURVE ( 'NONE', #3309, #18951, #4624, .T. ) ;
#3301=CARTESIAN_POINT ( 'NONE',  ( 5.078177448618336420, 0.000000000000000000, 0.000000000000000000 ) ) ;
#3302=TOROIDAL_SURFACE ( 'NONE', #21222, 10.94716442891539643, 0.2999999999999999334 ) ;
#3309=VERTEX_POINT ( 'NONE', #3494 ) ;
#3339=PLANE ( 'NONE',  #13083 ) ;
#3351=DIRECTION ( 'NONE',  ( -1.000000000000000000, 0.000000000000000000, -0.000000000000000000 ) ) ;
#3354=TOROIDAL_SURFACE ( 'NONE', #22855, 14.42592346043842433, 0.2999999999999999334 ) ;
#3494=CARTESIAN_POINT ( 'NONE',  ( 6.699999999999996625, 1.699310525220102153E-15, -13.72592346138681130 ) ) ;
#3519=ORIENTED_EDGE ( 'NONE', *, *, #12606, .T. ) ;
#3532=CARTESIAN_POINT ( 'NONE',  ( 0.9999999999999986677, 0.000000000000000000, 13.72592346138681130 ) ) ;
#3535=AXIS2_PLACEMENT_3D ( 'NONE', #16729, #14782, #9385 ) ;
#3564=CARTESIAN_POINT ( 'NONE',  ( 0.9999999999999986677, 11.22592346138681130, 0.000000000000000000 ) ) ;
#3603=ORIENTED_EDGE ( 'NONE', *, *, #23310, .F. ) ;
#3607=EDGE_LOOP ( 'NONE', ( #17880, #12437, #22439, #2706 ) ) ;
#3620=DIRECTION ( 'NONE',  ( -0.000000000000000000, 1.000000000000000000, 1.224646799147353207E-16 ) ) ;
#3664=AXIS2_PLACEMENT_3D ( 'NONE', #14671, #14417, #21652 ) ;
#3724=ADVANCED_FACE ( 'NONE', ( #4347 ), #18300, .T. ) ;
#3766=ORIENTED_EDGE ( 'NONE', *, *, #12254, .F. ) ;
#3904=DIRECTION ( 'NONE',  ( 0.000000000000000000, -1.224646799147353207E-16, 1.000000000000000000 ) ) ;
#3960=EDGE_CURVE ( 'NONE', #20194, #8068, #22111, .T. ) ;
#3967=LINE ( 'NONE', #17019, #6384 ) ;
#4008=AXIS2_PLACEMENT_3D ( 'NONE', #6907, #18244, #18135 ) ;
#4054=CIRCLE ( 'NONE', #13011, 0.9599481167642566204 ) ;
#4065=AXIS2_PLACEMENT_3D ( 'NONE', #16812, #22468, #5748 ) ;
#4145=AXIS2_PLACEMENT_3D ( 'NONE', #4989, #1670, #23871 ) ;
#4171=AXIS2_PLACEMENT_3D ( 'NONE', #17553, #10476, #23552 ) ;
#4194=VERTEX_POINT ( 'NONE', #21025 ) ;
#4198=EDGE_CURVE ( 'NONE', #18108, #4194, #10019, .T. ) ;
#4214=ORIENTED_EDGE ( 'NONE', *, *, #10870, .F. ) ;
#4261=CARTESIAN_POINT ( 'NONE',  ( 0.9999999999999986677, 0.000000000000000000, 11.22592346138681130 ) ) ;
#4282=DIRECTION ( 'NONE',  ( -1.000000000000000000, -0.000000000000000000, -0.000000000000000000 ) ) ;
#4316=ORIENTED_EDGE ( 'NONE', *, *, #19214, .F. ) ;
#4345=EDGE_CURVE ( 'NONE', #15317, #2103, #5213, .T. ) ;
#4347=FACE_OUTER_BOUND ( 'NONE', #11169, .T. ) ;
#4384=CONICAL_SURFACE ( 'NONE', #19197, 8.500000000000000000, 0.9519047898634274141 ) ;
#4389=ORIENTED_EDGE ( 'NONE', *, *, #11843, .T. ) ;
#4398=EDGE_CURVE ( 'NONE', #2976, #8087, #3967, .T. ) ;
#4406=CARTESIAN_POINT ( 'NONE',  ( 7.000000000000000888, 0.000000000000000000, 0.000000000000000000 ) ) ;
#4463=ORIENTED_EDGE ( 'NONE', *, *, #1025, .T. ) ;
#4464=ORIENTED_EDGE ( 'NONE', *, *, #22221, .F. ) ;
#4528=CIRCLE ( 'NONE', #22041, 0.2999999999999999334 ) ;
#4577=ADVANCED_FACE ( 'NONE', ( #11204, #3222 ), #18678, .F. ) ;
#4581=DIRECTION ( 'NONE',  ( -1.000000000000000000, -0.000000000000000000, -0.000000000000000000 ) ) ;
#4590=ORIENTED_EDGE ( 'NONE', *, *, #10272, .F. ) ;
#4604=DIRECTION ( 'NONE',  ( 0.000000000000000000, 0.000000000000000000, 1.000000000000000000 ) ) ;
#4608=ADVANCED_FACE ( 'NONE', ( #4962 ), #22477, .F. ) ;
#4624=CIRCLE ( 'NONE', #5379, 13.72592346138681130 ) ;
#4634=CARTESIAN_POINT ( 'NONE',  ( 0.2999999999999999334, 0.000000000000000000, 0.000000000000000000 ) ) ;
#4692=DIRECTION ( 'NONE',  ( -1.000000000000000000, -0.000000000000000000, -0.000000000000000000 ) ) ;
#4722=DIRECTION ( 'NONE',  ( -1.000000000000000000, -0.000000000000000000, -0.000000000000000000 ) ) ;
#4810=CARTESIAN_POINT ( 'NONE',  ( 0.000000000000000000, 1.803405503031483077E-15, -14.72592346043842326 ) ) ;
#4825=APPLICATION_CONTEXT ( 'automotive_design' ) ;
#4884=EDGE_CURVE ( 'NONE', #2345, #8087, #5238, .T. ) ;
#4962=FACE_OUTER_BOUND ( 'NONE', #23430, .T. ) ;
#4963=DIRECTION ( 'NONE',  ( 0.000000000000000000, 0.000000000000000000, 1.000000000000000000 ) ) ;
#4966=CARTESIAN_POINT ( 'NONE',  ( 6.999999999999999112, 0.000000000000000000, 0.000000000000000000 ) ) ;
#4989=CARTESIAN_POINT ( 'NONE',  ( 3.373806935227752118E-18, 0.000000000000000000, 0.000000000000000000 ) ) ;
#4997=CARTESIAN_POINT ( 'NONE',  ( 5.078177448618334644, 0.000000000000000000, 11.24716442891539714 ) ) ;
#5001=DIRECTION ( 'NONE',  ( 0.000000000000000000, 0.000000000000000000, -1.000000000000000000 ) ) ;
#5005=ORIENTED_EDGE ( 'NONE', *, *, #8731, .T. ) ;
#5014=DIRECTION ( 'NONE',  ( -1.000000000000000000, -0.000000000000000000, -0.000000000000000000 ) ) ;
#5056=DIRECTION ( 'NONE',  ( 0.000000000000000000, 0.000000000000000000, -1.000000000000000000 ) ) ;
#5074=LINE ( 'NONE', #14096, #61 ) ;
#5089=CYLINDRICAL_SURFACE ( 'NONE', #2980, 11.22592346138681130 ) ;
#5138=DIRECTION ( 'NONE',  ( -1.000000000000000000, -0.000000000000000000, -0.000000000000000000 ) ) ;
#5148=ORIENTED_EDGE ( 'NONE', *, *, #12510, .F. ) ;
#5153=AXIS2_PLACEMENT_3D ( 'NONE', #371, #9496, #3904 ) ;
#5161=AXIS2_PLACEMENT_3D ( 'NONE', #19683, #1245, #2957 ) ;
#5213=CIRCLE ( 'NONE', #7157, 9.725923461386811297 ) ;
#5223=CIRCLE ( 'NONE', #23935, 0.2999999999999999334 ) ;
#5238=CIRCLE ( 'NONE', #4065, 9.747164428915397139 ) ;
#5302=ORIENTED_EDGE ( 'NONE', *, *, #12606, .F. ) ;
#5304=ADVANCED_FACE ( 'NONE', ( #7418 ), #13820, .T. ) ;
#5361=CARTESIAN_POINT ( 'NONE',  ( 3.530011532367169913, 0.000000000000000000, 0.000000000000000000 ) ) ;
#5366=DIRECTION ( 'NONE',  ( -1.000000000000000000, -0.000000000000000000, -0.000000000000000000 ) ) ;
#5379=AXIS2_PLACEMENT_3D ( 'NONE', #18267, #16415, #23998 ) ;
#5413=EDGE_CURVE ( 'NONE', #15778, #2345, #16748, .T. ) ;
#5444=VERTEX_POINT ( 'NONE', #22264 ) ;
#5476=FACE_OUTER_BOUND ( 'NONE', #20842, .T. ) ;
#5501=ORIENTED_EDGE ( 'NONE', *, *, #19524, .F. ) ;
#5518=DIRECTION ( 'NONE',  ( -1.000000000000000000, 0.000000000000000000, -0.000000000000000000 ) ) ;
#5549=VECTOR ( 'NONE', #15996, 1000.000000000000000 ) ;
#5579=AXIS2_PLACEMENT_3D ( 'NONE', #13777, #483, #367 ) ;
#5605=ADVANCED_FACE ( 'NONE', ( #23371 ), #20396, .T. ) ;
#5690=ORIENTED_EDGE ( 'NONE', *, *, #762, .F. ) ;
#5718=AXIS2_PLACEMENT_3D ( 'NONE', #15658, #6414, #13859 ) ;
#5737=DIRECTION ( 'NONE',  ( -0.000000000000000000, 1.000000000000000000, 1.224646799147353207E-16 ) ) ;
#5748=DIRECTION ( 'NONE',  ( 0.000000000000000000, 0.000000000000000000, 1.000000000000000000 ) ) ;
#5791=CARTESIAN_POINT ( 'NONE',  ( 2.570122167802765922, 0.000000000000000000, 0.000000000000000000 ) ) ;
#5803=CARTESIAN_POINT ( 'NONE',  ( 2.570122167802765922, 0.000000000000000000, 0.000000000000000000 ) ) ;
#5868=EDGE_CURVE ( 'NONE', #2103, #15317, #23534, .T. ) ;
#5969=DIRECTION ( 'NONE',  ( 0.000000000000000000, -1.224646799147353207E-16, 1.000000000000000000 ) ) ;
#5978=CARTESIAN_POINT ( 'NONE',  ( 0.000000000000000000, 0.000000000000000000, 0.000000000000000000 ) ) ;
#6066=CARTESIAN_POINT ( 'NONE',  ( 0.000000000000000000, 0.000000000000000000, 0.000000000000000000 ) ) ;
#6067=DIRECTION ( 'NONE',  ( 0.000000000000000000, 0.000000000000000000, 1.000000000000000000 ) ) ;
#6098=DIRECTION ( 'NONE',  ( 0.000000000000000000, 0.000000000000000000, 1.000000000000000000 ) ) ;
#6123=AXIS2_PLACEMENT_3D ( 'NONE', #3085, #19556, #3190 ) ;
#6137=CYLINDRICAL_SURFACE ( 'NONE', #10331, 13.72592346138681130 ) ;
#6201=CARTESIAN_POINT ( 'NONE',  ( 0.2999999999999999334, 0.000000000000000000, 14.42592346043842433 ) ) ;
#6322=VECTOR ( 'NONE', #7672, 1000.000000000000000 ) ;
#6384=VECTOR ( 'NONE', #7734, 1000.000000000000114 ) ;
#6411=AXIS2_PLACEMENT_3D ( 'NONE', #6820, #23422, #5001 ) ;
#6414=DIRECTION ( 'NONE',  ( -1.000000000000000000, -0.000000000000000000, -0.000000000000000000 ) ) ;
#6458=DIRECTION ( 'NONE',  ( -1.000000000000000000, -0.000000000000000000, -0.000000000000000000 ) ) ;
#6538=ORIENTED_EDGE ( 'NONE', *, *, #19524, .T. ) ;
#6545=DIRECTION ( 'NONE',  ( 0.000000000000000000, 0.000000000000000000, 1.000000000000000000 ) ) ;
#6565=( NAMED_UNIT ( * ) SI_UNIT ( $, .STERADIAN. ) SOLID_ANGLE_UNIT ( ) );
#6643=FACE_OUTER_BOUND ( 'NONE', #17008, .T. ) ;
#6660=ORIENTED_EDGE ( 'NONE', *, *, #9989, .T. ) ;
#6661=DIRECTION ( 'NONE',  ( 1.000000000000000000, 0.000000000000000000, 0.000000000000000000 ) ) ;
#6664=CIRCLE ( 'NONE', #3535, 0.2999999999999999334 ) ;
#6681=ORIENTED_EDGE ( 'NONE', *, *, #1025, .F. ) ;
#6748=CIRCLE ( 'NONE', #19215, 11.24716442891539714 ) ;
#6767=AXIS2_PLACEMENT_3D ( 'NONE', #6883, #21767, #14890 ) ;
#6803=VERTEX_POINT ( 'NONE', #17568 ) ;
#6817=DIRECTION ( 'NONE',  ( 0.000000000000000000, 0.000000000000000000, 1.000000000000000000 ) ) ;
#6820=CARTESIAN_POINT ( 'NONE',  ( 6.699999999999999289, 0.000000000000000000, 14.02592346138681201 ) ) ;
#6880=ORIENTED_EDGE ( 'NONE', *, *, #5413, .T. ) ;
#6883=CARTESIAN_POINT ( 'NONE',  ( 0.000000000000000000, 0.000000000000000000, 0.000000000000000000 ) ) ;
#6884=ADVANCED_FACE ( 'NONE', ( #7395 ), #11403, .T. ) ;
#6899=DIRECTION ( 'NONE',  ( -0.000000000000000000, 0.000000000000000000, 1.000000000000000000 ) ) ;
#6905=FACE_OUTER_BOUND ( 'NONE', #514, .T. ) ;
#6906=CYLINDRICAL_SURFACE ( 'NONE', #7496, 13.72592346138681130 ) ;
#6907=CARTESIAN_POINT ( 'NONE',  ( 5.078177448618334644, 0.000000000000000000, 0.000000000000000000 ) ) ;
#6991=FACE_BOUND ( 'NONE', #19617, .T. ) ;
#6998=ORIENTED_EDGE ( 'NONE', *, *, #22221, .T. ) ;
#7003=ORIENTED_EDGE ( 'NONE', *, *, #11746, .T. ) ;
#7137=AXIS2_PLACEMENT_3D ( 'NONE', #23624, #1285, #4963 ) ;
#7153=VECTOR ( 'NONE', #10516, 1000.000000000000000 ) ;
#7157=AXIS2_PLACEMENT_3D ( 'NONE', #5803, #17134, #18623 ) ;
#7180=FACE_OUTER_BOUND ( 'NONE', #1652, .T. ) ;
#7224=AXIS2_PLACEMENT_3D ( 'NONE', #16944, #18667, #13403 ) ;
#7238=ORIENTED_EDGE ( 'NONE', *, *, #10561, .F. ) ;
#7282=DIRECTION ( 'NONE',  ( 0.000000000000000000, -1.224646799147353207E-16, 1.000000000000000000 ) ) ;
#7309=( NAMED_UNIT ( * ) PLANE_ANGLE_UNIT ( ) SI_UNIT ( $, .RADIAN. ) );
#7331=ORIENTED_EDGE ( 'NONE', *, *, #20280, .F. ) ;
#7347=EDGE_CURVE ( 'NONE', #11891, #13330, #23147, .T. ) ;
#7370=ADVANCED_FACE ( 'NONE', ( #6643 ), #4384, .F. ) ;
#7390=CYLINDRICAL_SURFACE ( 'NONE', #9401, 11.24716442891539714 ) ;
#7392=DIRECTION ( 'NONE',  ( -1.000000000000000000, -0.000000000000000000, -0.000000000000000000 ) ) ;
#7395=FACE_OUTER_BOUND ( 'NONE', #1439, .T. ) ;
#7402=ORIENTED_EDGE ( 'NONE', *, *, #12510, .T. ) ;
#7412=CARTESIAN_POINT ( 'NONE',  ( 5.378177448618336243, 0.000000000000000000, -9.747164428915397139 ) ) ;
#7418=FACE_OUTER_BOUND ( 'NONE', #22241, .T. ) ;
#7496=AXIS2_PLACEMENT_3D ( 'NONE', #3113, #19599, #17627 ) ;
#7519=AXIS2_PLACEMENT_3D ( 'NONE', #11870, #10028, #17487 ) ;
#7599=FACE_OUTER_BOUND ( 'NONE', #10219, .T. ) ;
#7601=ORIENTED_EDGE ( 'NONE', *, *, #984, .F. ) ;
#7605=ORIENTED_EDGE ( 'NONE', *, *, #23896, .T. ) ;
#7632=CARTESIAN_POINT ( 'NONE',  ( 6.699999999999999289, 0.000000000000000000, 0.000000000000000000 ) ) ;
#7672=DIRECTION ( 'NONE',  ( -1.000000000000000000, -0.000000000000000000, -0.000000000000000000 ) ) ;
#7694=EDGE_CURVE ( 'NONE', #21516, #1993, #2037, .T. ) ;
#7727=DIRECTION ( 'NONE',  ( -1.000000000000000000, -0.000000000000000000, -0.000000000000000000 ) ) ;
#7734=DIRECTION ( 'NONE',  ( 0.5801326495544486539, 9.975017754987290696E-17, 0.8145220125453549453 ) ) ;
#7752=CARTESIAN_POINT ( 'NONE',  ( 2.570122167802765922, 0.000000000000000000, 0.000000000000000000 ) ) ;
#7863=FACE_OUTER_BOUND ( 'NONE', #17341, .T. ) ;
#7886=EDGE_CURVE ( 'NONE', #8068, #20194, #17253, .T. ) ;
#7900=AXIS2_PLACEMENT_3D ( 'NONE', #12881, #7392, #14726 ) ;
#7916=EDGE_CURVE ( 'NONE', #19252, #5444, #23885, .T. ) ;
#7972=EDGE_CURVE ( 'NONE', #5444, #19252, #16096, .T. ) ;
#7983=CYLINDRICAL_SURFACE ( 'NONE', #11125, 9.725923461386811297 ) ;
#8005=AXIS2_PLACEMENT_3D ( 'NONE', #5978, #22344, #13412 ) ;
#8041=CARTESIAN_POINT ( 'NONE',  ( 5.078177448618336420, 0.000000000000000000, 0.000000000000000000 ) ) ;
#8059=CARTESIAN_POINT ( 'NONE',  ( 6.699999999999996625, 0.000000000000000000, 0.000000000000000000 ) ) ;
#8068=VERTEX_POINT ( 'NONE', #22485 ) ;
#8077=CARTESIAN_POINT ( 'NONE',  ( 3.530011532367169913, 0.000000000000000000, 0.000000000000000000 ) ) ;
#8087=VERTEX_POINT ( 'NONE', #19672 ) ;
#8130=ADVANCED_BREP_SHAPE_REPRESENTATION ( '', ( #18892, #8005 ), #1445 ) ;
#8143=CARTESIAN_POINT ( 'NONE',  ( 7.000000000000000888, 0.000000000000000000, 14.72592346043842326 ) ) ;
#8145=ORIENTED_EDGE ( 'NONE', *, *, #4198, .T. ) ;
#8300=EDGE_LOOP ( 'NONE', ( #2900, #408, #4389, #5148 ) ) ;
#8339=ORIENTED_EDGE ( 'NONE', *, *, #5868, .F. ) ;
#8389=TOROIDAL_SURFACE ( 'NONE', #7224, 14.02592346138681201, 0.2999999999999999334 ) ;
#8401=VERTEX_POINT ( 'NONE', #11429 ) ;
#8483=FACE_OUTER_BOUND ( 'NONE', #10002, .T. ) ;
#8542=VERTEX_POINT ( 'NONE', #10086 ) ;
#8595=DIRECTION ( 'NONE',  ( -0.8428161139095668997, 0.000000000000000000, 0.5382016333442104505 ) ) ;
#8643=PRODUCT_DEFINITION_SHAPE ( 'NONE', 'NONE',  #13603 ) ;
#8674=EDGE_CURVE ( 'NONE', #15584, #6803, #11394, .T. ) ;
#8692=DIRECTION ( 'NONE',  ( 1.000000000000000000, 0.000000000000000000, 0.000000000000000000 ) ) ;
#8731=EDGE_CURVE ( 'NONE', #379, #1993, #11012, .T. ) ;
#8770=AXIS2_PLACEMENT_3D ( 'NONE', #5791, #14804, #9415 ) ;
#8784=( NAMED_UNIT ( * ) SI_UNIT ( $, .STERADIAN. ) SOLID_ANGLE_UNIT ( ) );
#8787=DIRECTION ( 'NONE',  ( -1.000000000000000000, -0.000000000000000000, -0.000000000000000000 ) ) ;
#8805=CYLINDRICAL_SURFACE ( 'NONE', #6123, 14.72592346043842326 ) ;
#8862=DIRECTION ( 'NONE',  ( -1.000000000000000000, -0.000000000000000000, -0.000000000000000000 ) ) ;
#8980=ORIENTED_EDGE ( 'NONE', *, *, #7694, .F. ) ;
#9041=EDGE_LOOP ( 'NONE', ( #15872, #22085 ) ) ;
#9056=EDGE_LOOP ( 'NONE', ( #4316, #7402, #17254, #10469 ) ) ;
#9069=ORIENTED_EDGE ( 'NONE', *, *, #15585, .T. ) ;
#9144=CARTESIAN_POINT ( 'NONE',  ( 0.2999999999999999889, 0.000000000000000000, 0.000000000000000000 ) ) ;
#9164=CIRCLE ( 'NONE', #4171, 14.72592346043842326 ) ;
#9190=CIRCLE ( 'NONE', #4145, 10.02592346138681201 ) ;
#9261=ORIENTED_EDGE ( 'NONE', *, *, #15427, .F. ) ;
#9269=CARTESIAN_POINT ( 'NONE',  ( 0.000000000000000000, 0.000000000000000000, 0.000000000000000000 ) ) ;
#9325=EDGE_CURVE ( 'NONE', #2764, #21134, #21136, .T. ) ;
#9369=CARTESIAN_POINT ( 'NONE',  ( 5.078177448618336420, 0.000000000000000000, 10.94716442891539643 ) ) ;
#9385=DIRECTION ( 'NONE',  ( 0.000000000000000000, 0.000000000000000000, -1.000000000000000000 ) ) ;
#9401=AXIS2_PLACEMENT_3D ( 'NONE', #18744, #22293, #22540 ) ;
#9415=DIRECTION ( 'NONE',  ( 0.000000000000000000, 0.000000000000000000, 1.000000000000000000 ) ) ;
#9456=DIRECTION ( 'NONE',  ( -1.000000000000000000, -0.000000000000000000, -0.000000000000000000 ) ) ;
#9466=CIRCLE ( 'NONE', #13779, 14.72592346043842326 ) ;
#9496=DIRECTION ( 'NONE',  ( -0.000000000000000000, 1.000000000000000000, 1.224646799147353207E-16 ) ) ;
#9510=AXIS2_PLACEMENT_3D ( 'NONE', #21320, #13992, #1069 ) ;
#9555=PLANE ( 'NONE',  #14929 ) ;
#9653=FACE_OUTER_BOUND ( 'NONE', #18987, .T. ) ;
#9665=CARTESIAN_POINT ( 'NONE',  ( 4.489900896931573904, 0.000000000000000000, -8.500000000000000000 ) ) ;
#9740=DIRECTION ( 'NONE',  ( -1.000000000000000000, -0.000000000000000000, -0.000000000000000000 ) ) ;
#9784=ADVANCED_FACE ( 'NONE', ( #8483 ), #6906, .F. ) ;
#9792=TOROIDAL_SURFACE ( 'NONE', #22677, 10.94716442891539643, 0.2999999999999999334 ) ;
#9813=CIRCLE ( 'NONE', #14889, 10.02592346138681201 ) ;
#9849=ORIENTED_EDGE ( 'NONE', *, *, #23310, .T. ) ;
#9889=DIRECTION ( 'NONE',  ( -1.000000000000000000, -0.000000000000000000, -0.000000000000000000 ) ) ;
#9937=ORIENTED_EDGE ( 'NONE', *, *, #9325, .T. ) ;
#9989=EDGE_CURVE ( 'NONE', #21516, #2764, #22701, .T. ) ;
#10002=EDGE_LOOP ( 'NONE', ( #21485, #16788, #16631, #14505 ) ) ;
#10019=LINE ( 'NONE', #4810, #23312 ) ;
#10028=DIRECTION ( 'NONE',  ( -1.000000000000000000, -0.000000000000000000, -0.000000000000000000 ) ) ;
#10086=CARTESIAN_POINT ( 'NONE',  ( 0.3000000000000023204, 1.191082103573950144E-15, -9.725923461386809521 ) ) ;
#10137=ORIENTED_EDGE ( 'NONE', *, *, #11843, .F. ) ;
#10142=CARTESIAN_POINT ( 'NONE',  ( 0.3000000000000020983, 0.000000000000000000, 0.000000000000000000 ) ) ;
#10143=DIRECTION ( 'NONE',  ( 0.000000000000000000, 0.000000000000000000, 1.000000000000000000 ) ) ;
#10181=VERTEX_POINT ( 'NONE', #3532 ) ;
#10219=EDGE_LOOP ( 'NONE', ( #7238, #11230 ) ) ;
#10272=EDGE_CURVE ( 'NONE', #10181, #18733, #881, .T. ) ;
#10331=AXIS2_PLACEMENT_3D ( 'NONE', #13578, #774, #11483 ) ;
#10345=CARTESIAN_POINT ( 'NONE',  ( 3.530011532367169913, 1.376079757590787351E-15, -11.23654394515110511 ) ) ;
#10392=CARTESIAN_POINT ( 'NONE',  ( 0.000000000000000000, 0.000000000000000000, 11.22592346138681130 ) ) ;
#10394=ORIENTED_EDGE ( 'NONE', *, *, #17130, .T. ) ;
#10418=ORIENTED_EDGE ( 'NONE', *, *, #7916, .F. ) ;
#10426=CARTESIAN_POINT ( 'NONE',  ( 0.2999999999999999889, 0.000000000000000000, 0.000000000000000000 ) ) ;
#10444=ORIENTED_EDGE ( 'NONE', *, *, #7347, .T. ) ;
#10455=FACE_OUTER_BOUND ( 'NONE', #12247, .T. ) ;
#10469=ORIENTED_EDGE ( 'NONE', *, *, #7347, .F. ) ;
#10476=DIRECTION ( 'NONE',  ( -1.000000000000000000, -0.000000000000000000, -0.000000000000000000 ) ) ;
#10496=CIRCLE ( 'NONE', #18688, 11.24716442891539714 ) ;
#10516=DIRECTION ( 'NONE',  ( -1.000000000000000000, -0.000000000000000000, -0.000000000000000000 ) ) ;
#10561=EDGE_CURVE ( 'NONE', #6803, #15584, #10973, .T. ) ;
#10584=FACE_OUTER_BOUND ( 'NONE', #20801, .T. ) ;
#10598=( LENGTH_UNIT ( ) NAMED_UNIT ( * ) SI_UNIT ( .MILLI., .METRE. ) );
#10630=AXIS2_PLACEMENT_3D ( 'NONE', #8077, #4692, #10143 ) ;
#10709=CIRCLE ( 'NONE', #8770, 11.22592346138681130 ) ;
#10870=EDGE_CURVE ( 'NONE', #2976, #15317, #5074, .T. ) ;
#10937=LINE ( 'NONE', #24098, #17228 ) ;
#10973=CIRCLE ( 'NONE', #22320, 10.94716442891539465 ) ;
#10995=CARTESIAN_POINT ( 'NONE',  ( 4.489900896931573904, 0.000000000000000000, 0.000000000000000000 ) ) ;
#11012=CIRCLE ( 'NONE', #917, 0.9599481167642566204 ) ;
#11102=LINE ( 'NONE', #20055, #14552 ) ;
#11118=ORIENTED_EDGE ( 'NONE', *, *, #17469, .F. ) ;
#11125=AXIS2_PLACEMENT_3D ( 'NONE', #11634, #19105, #6545 ) ;
#11144=DIRECTION ( 'NONE',  ( 0.000000000000000000, 0.000000000000000000, -1.000000000000000000 ) ) ;
#11169=EDGE_LOOP ( 'NONE', ( #6681, #9849, #14787, #17692 ) ) ;
#11187=CARTESIAN_POINT ( 'NONE',  ( 6.999999999999999112, 0.000000000000000000, 14.02592346138681201 ) ) ;
#11204=FACE_OUTER_BOUND ( 'NONE', #9041, .T. ) ;
#11230=ORIENTED_EDGE ( 'NONE', *, *, #8674, .F. ) ;
#11268=FACE_OUTER_BOUND ( 'NONE', #15100, .T. ) ;
#11285=DIRECTION ( 'NONE',  ( 0.000000000000000000, 0.000000000000000000, 1.000000000000000000 ) ) ;
#11304=FACE_OUTER_BOUND ( 'NONE', #1003, .T. ) ;
#11394=CIRCLE ( 'NONE', #7900, 10.94716442891539465 ) ;
#11403=CYLINDRICAL_SURFACE ( 'NONE', #20782, 14.72592346043842326 ) ;
#11429=CARTESIAN_POINT ( 'NONE',  ( 4.489900896931573904, 1.377380391735520653E-15, -11.24716442891539359 ) ) ;
#11483=DIRECTION ( 'NONE',  ( 0.000000000000000000, 0.000000000000000000, 1.000000000000000000 ) ) ;
#11503=ADVANCED_FACE ( 'NONE', ( #19159 ), #9792, .T. ) ;
#11506=CIRCLE ( 'NONE', #1024, 13.72592346138681130 ) ;
#11528=EDGE_CURVE ( 'NONE', #15317, #16244, #13551, .T. ) ;
#11592=EDGE_LOOP ( 'NONE', ( #11970, #3519, #3766, #23006 ) ) ;
#11634=CARTESIAN_POINT ( 'NONE',  ( 0.000000000000000000, 0.000000000000000000, 0.000000000000000000 ) ) ;
#11686=CARTESIAN_POINT ( 'NONE',  ( 0.000000000000000000, 0.000000000000000000, 9.725923461386811297 ) ) ;
#11738=( GEOMETRIC_REPRESENTATION_CONTEXT ( 3 ) GLOBAL_UNCERTAINTY_ASSIGNED_CONTEXT ( ( #1087 ) ) GLOBAL_UNIT_ASSIGNED_CONTEXT ( ( #10598, #7309, #8784 ) ) REPRESENTATION_CONTEXT ( 'NONE', 'WORKASPACE' ) );
#11746=EDGE_CURVE ( 'NONE', #702, #23079, #9813, .T. ) ;
#11765=CIRCLE ( 'NONE', #16833, 8.500000000000000000 ) ;
#11815=DIRECTION ( 'NONE',  ( 0.000000000000000000, 0.000000000000000000, 1.000000000000000000 ) ) ;
#11824=AXIS2_PLACEMENT_3D ( 'NONE', #15011, #13437, #22490 ) ;
#11843=EDGE_CURVE ( 'NONE', #556, #13484, #10937, .T. ) ;
#11852=TOROIDAL_SURFACE ( 'NONE', #20457, 14.02592346138681201, 0.2999999999999999334 ) ;
#11861=ORIENTED_EDGE ( 'NONE', *, *, #11746, .F. ) ;
#11870=CARTESIAN_POINT ( 'NONE',  ( 0.000000000000000000, 0.000000000000000000, 0.000000000000000000 ) ) ;
#11891=VERTEX_POINT ( 'NONE', #12902 ) ;
#11914=AXIS2_PLACEMENT_3D ( 'NONE', #17716, #1016, #2961 ) ;
#11970=ORIENTED_EDGE ( 'NONE', *, *, #7916, .T. ) ;
#12058=ADVANCED_FACE ( 'NONE', ( #18347 ), #21890, .T. ) ;
#12219=ORIENTED_EDGE ( 'NONE', *, *, #4398, .T. ) ;
#12228=CIRCLE ( 'NONE', #6411, 0.2999999999999999334 ) ;
#12247=EDGE_LOOP ( 'NONE', ( #23617, #6660, #1610, #1716 ) ) ;
#12254=EDGE_CURVE ( 'NONE', #379, #8401, #6748, .T. ) ;
#12306=AXIS2_PLACEMENT_3D ( 'NONE', #23388, #6661, #14205 ) ;
#12346=ORIENTED_EDGE ( 'NONE', *, *, #21639, .T. ) ;
#12350=CARTESIAN_POINT ( 'NONE',  ( 0.000000000000000000, 1.680940823232891723E-15, -13.72592346138681130 ) ) ;
#12376=DIRECTION ( 'NONE',  ( 0.000000000000000000, 0.000000000000000000, 1.000000000000000000 ) ) ;
#12437=ORIENTED_EDGE ( 'NONE', *, *, #19214, .T. ) ;
#12475=ORIENTED_EDGE ( 'NONE', *, *, #9325, .F. ) ;
#12481=DIRECTION ( 'NONE',  ( -1.000000000000000000, -0.000000000000000000, -0.000000000000000000 ) ) ;
#12510=EDGE_CURVE ( 'NONE', #4194, #13484, #9466, .T. ) ;
#12567=CIRCLE ( 'NONE', #906, 14.42592346043842255 ) ;
#12606=EDGE_CURVE ( 'NONE', #5444, #8401, #15640, .T. ) ;
#12675=EDGE_CURVE ( 'NONE', #19252, #379, #11102, .T. ) ;
#12701=CARTESIAN_POINT ( 'NONE',  ( 6.699999999999999289, 1.717680227207312385E-15, -14.02592346138681201 ) ) ;
#12705=CIRCLE ( 'NONE', #11914, 9.747164428915397139 ) ;
#12722=AXIS2_PLACEMENT_3D ( 'NONE', #22089, #21833, #20004 ) ;
#12728=ADVANCED_FACE ( 'NONE', ( #20400 ), #1268, .T. ) ;
#12752=CARTESIAN_POINT ( 'NONE',  ( 4.489900896931573904, 0.000000000000000000, 11.24716442891539359 ) ) ;
#12761=FACE_OUTER_BOUND ( 'NONE', #9056, .T. ) ;
#12816=CARTESIAN_POINT ( 'NONE',  ( 5.378177448618336243, 1.359010689748310618E-15, -10.94716442891539465 ) ) ;
#12855=EDGE_CURVE ( 'NONE', #18108, #556, #14941, .T. ) ;
#12860=ORIENTED_EDGE ( 'NONE', *, *, #3295, .F. ) ;
#12881=CARTESIAN_POINT ( 'NONE',  ( 5.378177448618336243, 0.000000000000000000, 0.000000000000000000 ) ) ;
#12902=CARTESIAN_POINT ( 'NONE',  ( 0.000000000000000000, 1.785035801044272647E-15, -14.42592346043842255 ) ) ;
#12924=DIRECTION ( 'NONE',  ( -1.000000000000000000, -0.000000000000000000, -0.000000000000000000 ) ) ;
#12979=CARTESIAN_POINT ( 'NONE',  ( 0.000000000000000000, 0.000000000000000000, 14.42592346043842255 ) ) ;
#13011=AXIS2_PLACEMENT_3D ( 'NONE', #10345, #17925, #728 ) ;
#13018=ORIENTED_EDGE ( 'NONE', *, *, #5413, .F. ) ;
#13023=VECTOR ( 'NONE', #17114, 1000.000000000000114 ) ;
#13083=AXIS2_PLACEMENT_3D ( 'NONE', #3564, #5518, #18230 ) ;
#13121=CARTESIAN_POINT ( 'NONE',  ( 0.3000000000000023204, 0.000000000000000000, 9.725923461386809521 ) ) ;
#13149=CARTESIAN_POINT ( 'NONE',  ( 0.9999999999999986677, 0.000000000000000000, 0.000000000000000000 ) ) ;
#13153=ORIENTED_EDGE ( 'NONE', *, *, #5868, .T. ) ;
#13168=CARTESIAN_POINT ( 'NONE',  ( 0.000000000000000000, 0.000000000000000000, 0.000000000000000000 ) ) ;
#13189=ADVANCED_FACE ( 'NONE', ( #11304 ), #8389, .T. ) ;
#13193=APPLICATION_CONTEXT ( 'automotive_design' ) ;
#13203=ORIENTED_EDGE ( 'NONE', *, *, #20421, .T. ) ;
#13225=ORIENTED_EDGE ( 'NONE', *, *, #15525, .F. ) ;
#13239=ORIENTED_EDGE ( 'NONE', *, *, #10870, .T. ) ;
#13245=DIRECTION ( 'NONE',  ( 0.000000000000000000, 0.000000000000000000, 1.000000000000000000 ) ) ;
#13282=DIRECTION ( 'NONE',  ( 0.000000000000000000, 0.000000000000000000, 1.000000000000000000 ) ) ;
#13330=VERTEX_POINT ( 'NONE', #12979 ) ;
#13403=DIRECTION ( 'NONE',  ( 0.000000000000000000, 0.000000000000000000, 1.000000000000000000 ) ) ;
#13412=DIRECTION ( 'NONE',  ( 1.000000000000000000, 0.000000000000000000, 0.000000000000000000 ) ) ;
#13437=DIRECTION ( 'NONE',  ( -1.000000000000000000, -0.000000000000000000, -0.000000000000000000 ) ) ;
#13484=VERTEX_POINT ( 'NONE', #19827 ) ;
#13491=CIRCLE ( 'NONE', #5718, 9.725923461386809521 ) ;
#13549=DIRECTION ( 'NONE',  ( 0.000000000000000000, 0.000000000000000000, -1.000000000000000000 ) ) ;
#13551=LINE ( 'NONE', #11686, #6322 ) ;
#13578=CARTESIAN_POINT ( 'NONE',  ( 0.000000000000000000, 0.000000000000000000, 0.000000000000000000 ) ) ;
#13603=PRODUCT_DEFINITION ( 'UNKNOWN', '', #20904, #19127 ) ;
#13637=DIRECTION ( 'NONE',  ( 0.000000000000000000, -1.000000000000000000, 0.000000000000000000 ) ) ;
#13691=ADVANCED_FACE ( 'NONE', ( #20290, #6991 ), #3339, .F. ) ;
#13777=CARTESIAN_POINT ( 'NONE',  ( 5.078177448618334644, 0.000000000000000000, 0.000000000000000000 ) ) ;
#13779=AXIS2_PLACEMENT_3D ( 'NONE', #10142, #4581, #17599 ) ;
#13814=LINE ( 'NONE', #17467, #5549 ) ;
#13820=TOROIDAL_SURFACE ( 'NONE', #14587, 10.02592346138681023, 0.2999999999999999334 ) ;
#13839=ORIENTED_EDGE ( 'NONE', *, *, #681, .F. ) ;
#13859=DIRECTION ( 'NONE',  ( 0.000000000000000000, 0.000000000000000000, 1.000000000000000000 ) ) ;
#13890=ORIENTED_EDGE ( 'NONE', *, *, #681, .T. ) ;
#13938=ORIENTED_EDGE ( 'NONE', *, *, #17966, .F. ) ;
#13945=EDGE_LOOP ( 'NONE', ( #9261, #441, #2624, #21941 ) ) ;
#13976=EDGE_CURVE ( 'NONE', #8087, #2345, #12705, .T. ) ;
#13980=DIRECTION ( 'NONE',  ( 0.000000000000000000, 0.000000000000000000, 1.000000000000000000 ) ) ;
#13992=DIRECTION ( 'NONE',  ( -1.000000000000000000, -0.000000000000000000, -0.000000000000000000 ) ) ;
#14010=DIRECTION ( 'NONE',  ( -1.000000000000000000, -0.000000000000000000, -0.000000000000000000 ) ) ;
#14031=EDGE_LOOP ( 'NONE', ( #7331, #17433, #12346, #2807 ) ) ;
#14032=CARTESIAN_POINT ( 'NONE',  ( 4.489900896931573904, 0.000000000000000000, -8.500000000000000000 ) ) ;
#14076=CARTESIAN_POINT ( 'NONE',  ( 4.489900896931573904, 0.000000000000000000, 0.000000000000000000 ) ) ;
#14096=CARTESIAN_POINT ( 'NONE',  ( 2.570122167802765922, 0.000000000000000000, 9.725923461386811297 ) ) ;
#14122=CIRCLE ( 'NONE', #16445, 8.500000000000000000 ) ;
#14204=ORIENTED_EDGE ( 'NONE', *, *, #4884, .T. ) ;
#14205=DIRECTION ( 'NONE',  ( 0.000000000000000000, 0.000000000000000000, -1.000000000000000000 ) ) ;
#14221=EDGE_CURVE ( 'NONE', #13484, #4194, #9164, .T. ) ;
#14249=ADVANCED_FACE ( 'NONE', ( #10584 ), #23211, .T. ) ;
#14255=AXIS2_PLACEMENT_3D ( 'NONE', #17162, #14964, #11285 ) ;
#14321=ADVANCED_FACE ( 'NONE', ( #7180 ), #23275, .F. ) ;
#14348=DIRECTION ( 'NONE',  ( 0.000000000000000000, 0.000000000000000000, 1.000000000000000000 ) ) ;
#14417=DIRECTION ( 'NONE',  ( -1.000000000000000000, -0.000000000000000000, -0.000000000000000000 ) ) ;
#14505=ORIENTED_EDGE ( 'NONE', *, *, #10272, .T. ) ;
#14525=CARTESIAN_POINT ( 'NONE',  ( 0.000000000000000000, 1.191082103573950341E-15, -9.725923461386811297 ) ) ;
#14552=VECTOR ( 'NONE', #1742, 1000.000000000000000 ) ;
#14587=AXIS2_PLACEMENT_3D ( 'NONE', #9144, #14859, #22337 ) ;
#14671=CARTESIAN_POINT ( 'NONE',  ( 0.3000000000000023204, 0.000000000000000000, 0.000000000000000000 ) ) ;
#14678=ORIENTED_EDGE ( 'NONE', *, *, #4345, .T. ) ;
#14693=EDGE_CURVE ( 'NONE', #18733, #10181, #11506, .T. ) ;
#14716=ADVANCED_FACE ( 'NONE', ( #19598, #6905 ), #1062, .F. ) ;
#14726=DIRECTION ( 'NONE',  ( 0.000000000000000000, 0.000000000000000000, 1.000000000000000000 ) ) ;
#14782=DIRECTION ( 'NONE',  ( 0.000000000000000000, -1.000000000000000000, 0.000000000000000000 ) ) ;
#14787=ORIENTED_EDGE ( 'NONE', *, *, #17966, .T. ) ;
#14804=DIRECTION ( 'NONE',  ( -1.000000000000000000, -0.000000000000000000, -0.000000000000000000 ) ) ;
#14859=DIRECTION ( 'NONE',  ( -1.000000000000000000, -0.000000000000000000, -0.000000000000000000 ) ) ;
#14887=AXIS2_PLACEMENT_3D ( 'NONE', #13149, #20612, #18418 ) ;
#14889=AXIS2_PLACEMENT_3D ( 'NONE', #18656, #5366, #16797 ) ;
#14890=DIRECTION ( 'NONE',  ( 0.000000000000000000, 0.000000000000000000, 1.000000000000000000 ) ) ;
#14929=AXIS2_PLACEMENT_3D ( 'NONE', #15045, #22515, #18842 ) ;
#14941=CIRCLE ( 'NONE', #11824, 14.72592346043842326 ) ;
#14964=DIRECTION ( 'NONE',  ( -1.000000000000000000, -0.000000000000000000, -0.000000000000000000 ) ) ;
#14969=CARTESIAN_POINT ( 'NONE',  ( 4.489900896931573904, 1.117316575569334134E-15, 8.500000000000000000 ) ) ;
#14986=ORIENTED_EDGE ( 'NONE', *, *, #17849, .T. ) ;
#15011=CARTESIAN_POINT ( 'NONE',  ( 7.000000000000000888, 0.000000000000000000, 0.000000000000000000 ) ) ;
#15045=CARTESIAN_POINT ( 'NONE',  ( 5.378177448618336243, 9.747164428915397139, 0.000000000000000000 ) ) ;
#15100=EDGE_LOOP ( 'NONE', ( #5302, #15689, #16264, #5501 ) ) ;
#15127=EDGE_LOOP ( 'NONE', ( #18426, #1214 ) ) ;
#15282=LINE ( 'NONE', #10392, #1757 ) ;
#15293=ORIENTED_EDGE ( 'NONE', *, *, #8731, .F. ) ;
#15317=VERTEX_POINT ( 'NONE', #20681 ) ;
#15326=AXIS2_PLACEMENT_3D ( 'NONE', #9269, #12481, #1284 ) ;
#15427=EDGE_CURVE ( 'NONE', #3309, #8068, #16847, .T. ) ;
#15452=SHAPE_REPRESENTATION_RELATIONSHIP ( 'NONE' , 'NONE' ,  #852, #8130 ) ;
#15476=CARTESIAN_POINT ( 'NONE',  ( 6.999999999999999112, 0.000000000000000000, 0.000000000000000000 ) ) ;
#15525=EDGE_CURVE ( 'NONE', #2103, #8542, #18214, .T. ) ;
#15584=VERTEX_POINT ( 'NONE', #12816 ) ;
#15585=EDGE_CURVE ( 'NONE', #13330, #11891, #12567, .T. ) ;
#15632=AXIS2_PLACEMENT_3D ( 'NONE', #4634, #6458, #22931 ) ;
#15640=LINE ( 'NONE', #908, #7153 ) ;
#15656=CIRCLE ( 'NONE', #5153, 0.2999999999999999334 ) ;
#15658=CARTESIAN_POINT ( 'NONE',  ( 0.3000000000000023204, 0.000000000000000000, 0.000000000000000000 ) ) ;
#15673=DIRECTION ( 'NONE',  ( 0.000000000000000000, 0.000000000000000000, 1.000000000000000000 ) ) ;
#15689=ORIENTED_EDGE ( 'NONE', *, *, #7972, .T. ) ;
#15701=EDGE_CURVE ( 'NONE', #556, #18108, #21960, .T. ) ;
#15778=VERTEX_POINT ( 'NONE', #14032 ) ;
#15831=CONICAL_SURFACE ( 'NONE', #14255, 9.725923461386811297, 0.5683018928752935350 ) ;
#15857=AXIS2_PLACEMENT_3D ( 'NONE', #4966, #23970, #12376 ) ;
#15872=ORIENTED_EDGE ( 'NONE', *, *, #15701, .F. ) ;
#15902=LINE ( 'NONE', #12350, #2255 ) ;
#15952=CARTESIAN_POINT ( 'NONE',  ( 0.9999999999999986677, 0.000000000000000000, 0.000000000000000000 ) ) ;
#15958=DIRECTION ( 'NONE',  ( -1.000000000000000000, -0.000000000000000000, -0.000000000000000000 ) ) ;
#15996=DIRECTION ( 'NONE',  ( -0.8428161139095668997, 6.591069075708646964E-17, -0.5382016333442104505 ) ) ;
#16001=FACE_OUTER_BOUND ( 'NONE', #8300, .T. ) ;
#16016=CONICAL_SURFACE ( 'NONE', #2771, 9.725923461386811297, 0.5683018928752935350 ) ;
#16096=CIRCLE ( 'NONE', #4008, 11.24716442891539714 ) ;
#16196=CARTESIAN_POINT ( 'NONE',  ( 0.000000000000000000, 0.000000000000000000, 0.000000000000000000 ) ) ;
#16244=VERTEX_POINT ( 'NONE', #13121 ) ;
#16264=ORIENTED_EDGE ( 'NONE', *, *, #12675, .T. ) ;
#16415=DIRECTION ( 'NONE',  ( -1.000000000000000000, -0.000000000000000000, -0.000000000000000000 ) ) ;
#16445=AXIS2_PLACEMENT_3D ( 'NONE', #16850, #22720, #18950 ) ;
#16551=CARTESIAN_POINT ( 'NONE',  ( 0.2999999999999999334, 1.766666099057062414E-15, -14.42592346043842433 ) ) ;
#16617=AXIS2_PLACEMENT_3D ( 'NONE', #8059, #9889, #17465 ) ;
#16631=ORIENTED_EDGE ( 'NONE', *, *, #984, .T. ) ;
#16678=DIRECTION ( 'NONE',  ( 0.000000000000000000, -1.000000000000000000, 0.000000000000000000 ) ) ;
#16696=DIRECTION ( 'NONE',  ( -1.000000000000000000, -0.000000000000000000, -0.000000000000000000 ) ) ;
#16722=CARTESIAN_POINT ( 'NONE',  ( 2.570122167802765922, 1.191082103573950341E-15, -9.725923461386811297 ) ) ;
#16729=CARTESIAN_POINT ( 'NONE',  ( 0.2999999999999999889, 0.000000000000000000, 10.02592346138681023 ) ) ;
#16748=LINE ( 'NONE', #9665, #13023 ) ;
#16787=STYLED_ITEM('',(#24162),#18892);
#16788=ORIENTED_EDGE ( 'NONE', *, *, #23896, .F. ) ;
#16797=DIRECTION ( 'NONE',  ( 0.000000000000000000, 0.000000000000000000, 1.000000000000000000 ) ) ;
#16812=CARTESIAN_POINT ( 'NONE',  ( 5.378177448618336243, 0.000000000000000000, 0.000000000000000000 ) ) ;
#16818=VECTOR ( 'NONE', #5138, 1000.000000000000000 ) ;
#16820=DIRECTION ( 'NONE',  ( 0.000000000000000000, -1.000000000000000000, 0.000000000000000000 ) ) ;
#16833=AXIS2_PLACEMENT_3D ( 'NONE', #19314, #12924, #24049 ) ;
#16841=DIRECTION ( 'NONE',  ( -1.000000000000000000, -0.000000000000000000, -0.000000000000000000 ) ) ;
#16847=CIRCLE ( 'NONE', #518, 0.2999999999999999334 ) ;
#16850=CARTESIAN_POINT ( 'NONE',  ( 4.489900896931573904, 0.000000000000000000, 0.000000000000000000 ) ) ;
#16861=DIRECTION ( 'NONE',  ( -1.000000000000000000, -0.000000000000000000, -0.000000000000000000 ) ) ;
#16863=AXIS2_PLACEMENT_3D ( 'NONE', #22367, #16841, #20763 ) ;
#16875=EDGE_CURVE ( 'NONE', #13484, #13330, #20852, .T. ) ;
#16944=CARTESIAN_POINT ( 'NONE',  ( 6.699999999999999289, 0.000000000000000000, 0.000000000000000000 ) ) ;
#16956=DIRECTION ( 'NONE',  ( -1.000000000000000000, -0.000000000000000000, -0.000000000000000000 ) ) ;
#17006=FACE_BOUND ( 'NONE', #83, .T. ) ;
#17008=EDGE_LOOP ( 'NONE', ( #17920, #13890, #6880, #18445 ) ) ;
#17019=CARTESIAN_POINT ( 'NONE',  ( 4.489900896931573904, 1.040949779275250140E-15, 8.500000000000000000 ) ) ;
#17034=DIRECTION ( 'NONE',  ( 0.000000000000000000, 0.000000000000000000, 1.000000000000000000 ) ) ;
#17059=EDGE_LOOP ( 'NONE', ( #19226, #17809, #10418, #22917 ) ) ;
#17075=ADVANCED_FACE ( 'NONE', ( #99 ), #11852, .T. ) ;
#17114=DIRECTION ( 'NONE',  ( 0.5801326495544486539, 0.000000000000000000, -0.8145220125453549453 ) ) ;
#17130=EDGE_CURVE ( 'NONE', #21134, #2764, #18510, .T. ) ;
#17134=DIRECTION ( 'NONE',  ( -1.000000000000000000, -0.000000000000000000, -0.000000000000000000 ) ) ;
#17162=CARTESIAN_POINT ( 'NONE',  ( 2.570122167802765922, 0.000000000000000000, 0.000000000000000000 ) ) ;
#17228=VECTOR ( 'NONE', #16696, 1000.000000000000000 ) ;
#17253=CIRCLE ( 'NONE', #21564, 14.02592346138681201 ) ;
#17254=ORIENTED_EDGE ( 'NONE', *, *, #16875, .T. ) ;
#17255=ORIENTED_EDGE ( 'NONE', *, *, #14221, .F. ) ;
#17275=DIRECTION ( 'NONE',  ( -1.000000000000000000, -0.000000000000000000, -0.000000000000000000 ) ) ;
#17341=EDGE_LOOP ( 'NONE', ( #5690, #13839, #13239, #14678 ) ) ;
#17433=ORIENTED_EDGE ( 'NONE', *, *, #8674, .T. ) ;
#17464=ADVANCED_FACE ( 'NONE', ( #7599, #17006 ), #9555, .F. ) ;
#17465=DIRECTION ( 'NONE',  ( 0.000000000000000000, 0.000000000000000000, 1.000000000000000000 ) ) ;
#17467=CARTESIAN_POINT ( 'NONE',  ( 2.570122167802765922, 1.191082103573950341E-15, -9.725923461386811297 ) ) ;
#17469=EDGE_CURVE ( 'NONE', #1993, #21516, #10709, .T. ) ;
#17487=DIRECTION ( 'NONE',  ( 0.000000000000000000, 0.000000000000000000, 1.000000000000000000 ) ) ;
#17538=FACE_OUTER_BOUND ( 'NONE', #3607, .T. ) ;
#17548=DIRECTION ( 'NONE',  ( -1.000000000000000000, -0.000000000000000000, -0.000000000000000000 ) ) ;
#17553=CARTESIAN_POINT ( 'NONE',  ( 0.3000000000000020983, 0.000000000000000000, 0.000000000000000000 ) ) ;
#17568=CARTESIAN_POINT ( 'NONE',  ( 5.378177448618336243, 0.000000000000000000, 10.94716442891539465 ) ) ;
#17599=DIRECTION ( 'NONE',  ( 0.000000000000000000, 0.000000000000000000, 1.000000000000000000 ) ) ;
#17627=DIRECTION ( 'NONE',  ( 0.000000000000000000, 0.000000000000000000, 1.000000000000000000 ) ) ;
#17692=ORIENTED_EDGE ( 'NONE', *, *, #17849, .F. ) ;
#17711=ORIENTED_EDGE ( 'NONE', *, *, #4884, .F. ) ;
#17716=CARTESIAN_POINT ( 'NONE',  ( 5.378177448618336243, 0.000000000000000000, 0.000000000000000000 ) ) ;
#17809=ORIENTED_EDGE ( 'NONE', *, *, #20280, .T. ) ;
#17849=EDGE_CURVE ( 'NONE', #8542, #16244, #23169, .T. ) ;
#17880=ORIENTED_EDGE ( 'NONE', *, *, #14221, .T. ) ;
#17899=CLOSED_SHELL ( 'NONE', ( #6884, #19018, #5304, #4608, #21992, #14321, #11503, #12728, #14249, #23287, #22668, #13189, #4577, #17075, #9784, #13691, #12058, #5605, #19358, #2428, #17464, #7370, #18332, #23610, #3724, #14716, #23339, #22803 ) ) ;
#17920=ORIENTED_EDGE ( 'NONE', *, *, #4398, .F. ) ;
#17925=DIRECTION ( 'NONE',  ( -0.000000000000000000, 1.000000000000000000, 1.224646799147353207E-16 ) ) ;
#17966=EDGE_CURVE ( 'NONE', #702, #16244, #6664, .T. ) ;
#17990=CARTESIAN_POINT ( 'NONE',  ( 7.000000000000000000, 14.02592346138681378, 0.000000000000000000 ) ) ;
#17998=CARTESIAN_POINT ( 'NONE',  ( 0.9999999999999986677, 0.000000000000000000, 0.000000000000000000 ) ) ;
#18043=VECTOR ( 'NONE', #1503, 1000.000000000000000 ) ;
#18108=VERTEX_POINT ( 'NONE', #21122 ) ;
#18135=DIRECTION ( 'NONE',  ( 0.000000000000000000, 0.000000000000000000, 1.000000000000000000 ) ) ;
#18214=LINE ( 'NONE', #14525, #18043 ) ;
#18230=DIRECTION ( 'NONE',  ( -0.000000000000000000, 0.000000000000000000, 1.000000000000000000 ) ) ;
#18244=DIRECTION ( 'NONE',  ( -1.000000000000000000, -0.000000000000000000, -0.000000000000000000 ) ) ;
#18266=CARTESIAN_POINT ( 'NONE',  ( 0.2999999999999999334, 0.000000000000000000, 0.000000000000000000 ) ) ;
#18267=CARTESIAN_POINT ( 'NONE',  ( 6.699999999999996625, 0.000000000000000000, 0.000000000000000000 ) ) ;
#18300=TOROIDAL_SURFACE ( 'NONE', #22577, 10.02592346138681023, 0.2999999999999999334 ) ;
#18332=ADVANCED_FACE ( 'NONE', ( #7863 ), #16016, .F. ) ;
#18347=FACE_OUTER_BOUND ( 'NONE', #2663, .T. ) ;
#18405=AXIS2_PLACEMENT_3D ( 'NONE', #16551, #3620, #7282 ) ;
#18418=DIRECTION ( 'NONE',  ( 0.000000000000000000, 0.000000000000000000, 1.000000000000000000 ) ) ;
#18426=ORIENTED_EDGE ( 'NONE', *, *, #3960, .T. ) ;
#18445=ORIENTED_EDGE ( 'NONE', *, *, #13976, .F. ) ;
#18455=AXIS2_PLACEMENT_3D ( 'NONE', #4406, #4282, #11815 ) ;
#18510=CIRCLE ( 'NONE', #9510, 11.22592346138681130 ) ;
#18568=CARTESIAN_POINT ( 'NONE',  ( 0.000000000000000000, 0.000000000000000000, 13.72592346138681130 ) ) ;
#18623=DIRECTION ( 'NONE',  ( 0.000000000000000000, 0.000000000000000000, 1.000000000000000000 ) ) ;
#18656=CARTESIAN_POINT ( 'NONE',  ( 3.373806935227752118E-18, 0.000000000000000000, 0.000000000000000000 ) ) ;
#18667=DIRECTION ( 'NONE',  ( -1.000000000000000000, -0.000000000000000000, -0.000000000000000000 ) ) ;
#18678=PLANE ( 'NONE',  #2476 ) ;
#18685=ORIENTED_EDGE ( 'NONE', *, *, #3960, .F. ) ;
#18688=AXIS2_PLACEMENT_3D ( 'NONE', #811, #4722, #15673 ) ;
#18733=VERTEX_POINT ( 'NONE', #23332 ) ;
#18744=CARTESIAN_POINT ( 'NONE',  ( 0.000000000000000000, 0.000000000000000000, 0.000000000000000000 ) ) ;
#18755=ORIENTED_EDGE ( 'NONE', *, *, #20421, .F. ) ;
#18842=DIRECTION ( 'NONE',  ( -0.000000000000000000, 0.000000000000000000, 1.000000000000000000 ) ) ;
#18892=MANIFOLD_SOLID_BREP ( 'Revolve1', #17899 ) ;
#18950=DIRECTION ( 'NONE',  ( 0.000000000000000000, 0.000000000000000000, 1.000000000000000000 ) ) ;
#18951=VERTEX_POINT ( 'NONE', #20723 ) ;
#18987=EDGE_LOOP ( 'NONE', ( #12860, #19854, #2193, #7601 ) ) ;
#19018=ADVANCED_FACE ( 'NONE', ( #17538 ), #76, .T. ) ;
#19105=DIRECTION ( 'NONE',  ( -1.000000000000000000, -0.000000000000000000, -0.000000000000000000 ) ) ;
#19127=PRODUCT_DEFINITION_CONTEXT ( 'detailed design', #13193, 'design' ) ;
#19133=DIRECTION ( 'NONE',  ( 0.000000000000000000, 0.000000000000000000, -1.000000000000000000 ) ) ;
#19159=FACE_OUTER_BOUND ( 'NONE', #17059, .T. ) ;
#19197=AXIS2_PLACEMENT_3D ( 'NONE', #14076, #8692, #5056 ) ;
#19214=EDGE_CURVE ( 'NONE', #4194, #11891, #1261, .T. ) ;
#19215=AXIS2_PLACEMENT_3D ( 'NONE', #10995, #16861, #179 ) ;
#19226=ORIENTED_EDGE ( 'NONE', *, *, #10561, .T. ) ;
#19252=VERTEX_POINT ( 'NONE', #4997 ) ;
#19253=( LENGTH_UNIT ( ) NAMED_UNIT ( * ) SI_UNIT ( .MILLI., .METRE. ) );
#19314=CARTESIAN_POINT ( 'NONE',  ( 4.489900896931573904, 0.000000000000000000, 0.000000000000000000 ) ) ;
#19358=ADVANCED_FACE ( 'NONE', ( #11268 ), #7390, .T. ) ;
#19524=EDGE_CURVE ( 'NONE', #8401, #379, #10496, .T. ) ;
#19556=DIRECTION ( 'NONE',  ( -1.000000000000000000, -0.000000000000000000, -0.000000000000000000 ) ) ;
#19558=ORIENTED_EDGE ( 'NONE', *, *, #9989, .F. ) ;
#19598=FACE_BOUND ( 'NONE', #2818, .T. ) ;
#19599=DIRECTION ( 'NONE',  ( -1.000000000000000000, -0.000000000000000000, -0.000000000000000000 ) ) ;
#19617=EDGE_LOOP ( 'NONE', ( #10394, #9937 ) ) ;
#19672=CARTESIAN_POINT ( 'NONE',  ( 5.378177448618336243, 1.193683371863418128E-15, 9.747164428915397139 ) ) ;
#19683=CARTESIAN_POINT ( 'NONE',  ( 2.570122167802765922, 0.000000000000000000, 0.000000000000000000 ) ) ;
#19766=CARTESIAN_POINT ( 'NONE',  ( 5.378177448618336243, 0.000000000000000000, 0.000000000000000000 ) ) ;
#19827=CARTESIAN_POINT ( 'NONE',  ( 0.3000000000000020983, 0.000000000000000000, 14.72592346043842326 ) ) ;
#19854=ORIENTED_EDGE ( 'NONE', *, *, #1883, .T. ) ;
#19968=PRODUCT_CONTEXT ( 'NONE', #4825, 'mechanical' ) ;
#19976=DIRECTION ( 'NONE',  ( -1.000000000000000000, -0.000000000000000000, -0.000000000000000000 ) ) ;
#20004=DIRECTION ( 'NONE',  ( 0.000000000000000000, 0.000000000000000000, -1.000000000000000000 ) ) ;
#20041=DIRECTION ( 'NONE',  ( -0.000000000000000000, 1.000000000000000000, 1.224646799147353207E-16 ) ) ;
#20055=CARTESIAN_POINT ( 'NONE',  ( 0.000000000000000000, 0.000000000000000000, 11.24716442891539714 ) ) ;
#20167=DIRECTION ( 'NONE',  ( 0.000000000000000000, -1.224646799147353207E-16, 1.000000000000000000 ) ) ;
#20194=VERTEX_POINT ( 'NONE', #11187 ) ;
#20224=ORIENTED_EDGE ( 'NONE', *, *, #11528, .F. ) ;
#20280=EDGE_CURVE ( 'NONE', #15584, #5444, #5223, .T. ) ;
#20290=FACE_OUTER_BOUND ( 'NONE', #2928, .T. ) ;
#20392=EDGE_CURVE ( 'NONE', #18951, #20194, #12228, .T. ) ;
#20396=TOROIDAL_SURFACE ( 'NONE', #10630, 11.23654394515110511, 0.9599481167642566204 ) ;
#20400=FACE_OUTER_BOUND ( 'NONE', #11592, .T. ) ;
#20421=EDGE_CURVE ( 'NONE', #8401, #21516, #4054, .T. ) ;
#20457=AXIS2_PLACEMENT_3D ( 'NONE', #7632, #17275, #17034 ) ;
#20470=DIRECTION ( 'NONE',  ( -1.000000000000000000, -0.000000000000000000, -0.000000000000000000 ) ) ;
#20544=ORIENTED_EDGE ( 'NONE', *, *, #13976, .T. ) ;
#20612=DIRECTION ( 'NONE',  ( -1.000000000000000000, -0.000000000000000000, -0.000000000000000000 ) ) ;
#20681=CARTESIAN_POINT ( 'NONE',  ( 2.570122167802765922, 0.000000000000000000, 9.725923461386811297 ) ) ;
#20723=CARTESIAN_POINT ( 'NONE',  ( 6.699999999999996625, 0.000000000000000000, 13.72592346138681130 ) ) ;
#20763=DIRECTION ( 'NONE',  ( 0.000000000000000000, 0.000000000000000000, 1.000000000000000000 ) ) ;
#20782=AXIS2_PLACEMENT_3D ( 'NONE', #6066, #20470, #13245 ) ;
#20801=EDGE_LOOP ( 'NONE', ( #23286, #13203, #11118, #15293 ) ) ;
#20842=EDGE_LOOP ( 'NONE', ( #22288, #22625, #13153, #4214 ) ) ;
#20850=UNCERTAINTY_MEASURE_WITH_UNIT (LENGTH_MEASURE( 1.000000000000000082E-05 ), #19253, 'distance_accuracy_value', 'NONE');
#20852=CIRCLE ( 'NONE', #23593, 0.2999999999999999334 ) ;
#20904=PRODUCT_DEFINITION_FORMATION_WITH_SPECIFIED_SOURCE ( 'ANY', '', #23684, .NOT_KNOWN. ) ;
#20913=CIRCLE ( 'NONE', #16617, 13.72592346138681130 ) ;
#21025=CARTESIAN_POINT ( 'NONE',  ( 0.3000000000000020983, 1.803405503031483077E-15, -14.72592346043842326 ) ) ;
#21122=CARTESIAN_POINT ( 'NONE',  ( 7.000000000000000888, 1.803405503031483077E-15, -14.72592346043842326 ) ) ;
#21134=VERTEX_POINT ( 'NONE', #4261 ) ;
#21136=CIRCLE ( 'NONE', #22317, 11.22592346138681130 ) ;
#21222=AXIS2_PLACEMENT_3D ( 'NONE', #3301, #8787, #21711 ) ;
#21297=ORIENTED_EDGE ( 'NONE', *, *, #4345, .F. ) ;
#21320=CARTESIAN_POINT ( 'NONE',  ( 0.9999999999999986677, 0.000000000000000000, 0.000000000000000000 ) ) ;
#21330=( NAMED_UNIT ( * ) PLANE_ANGLE_UNIT ( ) SI_UNIT ( $, .RADIAN. ) );
#21342=EDGE_CURVE ( 'NONE', #1993, #21134, #15282, .T. ) ;
#21371=CARTESIAN_POINT ( 'NONE',  ( 0.000000000000000000, 1.374779123446053458E-15, -11.22592346138681130 ) ) ;
#21485=ORIENTED_EDGE ( 'NONE', *, *, #1883, .F. ) ;
#21516=VERTEX_POINT ( 'NONE', #22349 ) ;
#21564=AXIS2_PLACEMENT_3D ( 'NONE', #15476, #17548, #6098 ) ;
#21639=EDGE_CURVE ( 'NONE', #6803, #19252, #4528, .T. ) ;
#21652=DIRECTION ( 'NONE',  ( 0.000000000000000000, 0.000000000000000000, 1.000000000000000000 ) ) ;
#21698=DIRECTION ( 'NONE',  ( 0.000000000000000000, 0.000000000000000000, 1.000000000000000000 ) ) ;
#21711=DIRECTION ( 'NONE',  ( 0.000000000000000000, 0.000000000000000000, 1.000000000000000000 ) ) ;
#21767=DIRECTION ( 'NONE',  ( -1.000000000000000000, -0.000000000000000000, -0.000000000000000000 ) ) ;
#21833=DIRECTION ( 'NONE',  ( 1.000000000000000000, 0.000000000000000000, 0.000000000000000000 ) ) ;
#21890=CYLINDRICAL_SURFACE ( 'NONE', #7137, 11.22592346138681130 ) ;
#21941=ORIENTED_EDGE ( 'NONE', *, *, #7886, .F. ) ;
#21960=CIRCLE ( 'NONE', #18455, 14.72592346043842326 ) ;
#21968=VECTOR ( 'NONE', #9740, 1000.000000000000000 ) ;
#21992=ADVANCED_FACE ( 'NONE', ( #5476 ), #15831, .F. ) ;
#22041=AXIS2_PLACEMENT_3D ( 'NONE', #9369, #16820, #13549 ) ;
#22085=ORIENTED_EDGE ( 'NONE', *, *, #12855, .F. ) ;
#22089=CARTESIAN_POINT ( 'NONE',  ( 4.489900896931573904, 0.000000000000000000, 0.000000000000000000 ) ) ;
#22111=CIRCLE ( 'NONE', #15857, 14.02592346138681201 ) ;
#22221=EDGE_CURVE ( 'NONE', #16244, #8542, #13491, .T. ) ;
#22241=EDGE_LOOP ( 'NONE', ( #7003, #4463, #4464, #13938 ) ) ;
#22264=CARTESIAN_POINT ( 'NONE',  ( 5.078177448618334644, 1.377380391735521048E-15, -11.24716442891539714 ) ) ;
#22288=ORIENTED_EDGE ( 'NONE', *, *, #872, .F. ) ;
#22293=DIRECTION ( 'NONE',  ( -1.000000000000000000, -0.000000000000000000, -0.000000000000000000 ) ) ;
#22317=AXIS2_PLACEMENT_3D ( 'NONE', #15952, #14010, #3038 ) ;
#22320=AXIS2_PLACEMENT_3D ( 'NONE', #19766, #15958, #6817 ) ;
#22337=DIRECTION ( 'NONE',  ( 0.000000000000000000, 0.000000000000000000, 1.000000000000000000 ) ) ;
#22344=DIRECTION ( 'NONE',  ( 0.000000000000000000, 0.000000000000000000, 1.000000000000000000 ) ) ;
#22349=CARTESIAN_POINT ( 'NONE',  ( 2.570122167802765922, 1.374779123446053458E-15, -11.22592346138681130 ) ) ;
#22367=CARTESIAN_POINT ( 'NONE',  ( 2.570122167802765922, 0.000000000000000000, 0.000000000000000000 ) ) ;
#22439=ORIENTED_EDGE ( 'NONE', *, *, #15585, .F. ) ;
#22468=DIRECTION ( 'NONE',  ( -1.000000000000000000, -0.000000000000000000, -0.000000000000000000 ) ) ;
#22477=CYLINDRICAL_SURFACE ( 'NONE', #15326, 9.725923461386811297 ) ;
#22485=CARTESIAN_POINT ( 'NONE',  ( 6.999999999999999112, 1.717680227207312385E-15, -14.02592346138681201 ) ) ;
#22490=DIRECTION ( 'NONE',  ( 0.000000000000000000, 0.000000000000000000, 1.000000000000000000 ) ) ;
#22515=DIRECTION ( 'NONE',  ( -1.000000000000000000, 0.000000000000000000, -0.000000000000000000 ) ) ;
#22540=DIRECTION ( 'NONE',  ( 0.000000000000000000, 0.000000000000000000, 1.000000000000000000 ) ) ;
#22574=DIRECTION ( 'NONE',  ( -1.000000000000000000, -0.000000000000000000, -0.000000000000000000 ) ) ;
#22577=AXIS2_PLACEMENT_3D ( 'NONE', #10426, #2873, #13980 ) ;
#22625=ORIENTED_EDGE ( 'NONE', *, *, #762, .T. ) ;
#22668=ADVANCED_FACE ( 'NONE', ( #9653 ), #6137, .F. ) ;
#22671=MECHANICAL_DESIGN_GEOMETRIC_PRESENTATION_REPRESENTATION('',(#16787),#11738);
#22677=AXIS2_PLACEMENT_3D ( 'NONE', #8041, #16956, #270 ) ;
#22701=LINE ( 'NONE', #21371, #21968 ) ;
#22720=DIRECTION ( 'NONE',  ( -1.000000000000000000, -0.000000000000000000, -0.000000000000000000 ) ) ;
#22803=ADVANCED_FACE ( 'NONE', ( #16001 ), #8805, .T. ) ;
#22855=AXIS2_PLACEMENT_3D ( 'NONE', #18266, #8862, #14348 ) ;
#22859=CARTESIAN_POINT ( 'NONE',  ( 2.879195777975148768E-17, 0.000000000000000000, 10.02592346138681023 ) ) ;
#22868=ORIENTED_EDGE ( 'NONE', *, *, #15525, .T. ) ;
#22917=ORIENTED_EDGE ( 'NONE', *, *, #21639, .F. ) ;
#22931=DIRECTION ( 'NONE',  ( 0.000000000000000000, 0.000000000000000000, 1.000000000000000000 ) ) ;
#22956=ORIENTED_EDGE ( 'NONE', *, *, #20392, .F. ) ;
#22979=ORIENTED_EDGE ( 'NONE', *, *, #11528, .T. ) ;
#23006=ORIENTED_EDGE ( 'NONE', *, *, #12675, .F. ) ;
#23079=VERTEX_POINT ( 'NONE', #595 ) ;
#23147=CIRCLE ( 'NONE', #7519, 14.42592346043842255 ) ;
#23169=CIRCLE ( 'NONE', #3664, 9.725923461386809521 ) ;
#23179=ORIENTED_EDGE ( 'NONE', *, *, #21342, .T. ) ;
#23211=TOROIDAL_SURFACE ( 'NONE', #1451, 11.23654394515110511, 0.9599481167642566204 ) ;
#23271=FACE_OUTER_BOUND ( 'NONE', #314, .T. ) ;
#23275=CONICAL_SURFACE ( 'NONE', #12722, 8.500000000000000000, 0.9519047898634274141 ) ;
#23286=ORIENTED_EDGE ( 'NONE', *, *, #12254, .T. ) ;
#23287=ADVANCED_FACE ( 'NONE', ( #10455 ), #5089, .T. ) ;
#23310=EDGE_CURVE ( 'NONE', #23079, #702, #9190, .T. ) ;
#23312=VECTOR ( 'NONE', #2839, 1000.000000000000000 ) ;
#23332=CARTESIAN_POINT ( 'NONE',  ( 0.9999999999999986677, 1.680940823232891723E-15, -13.72592346138681130 ) ) ;
#23339=ADVANCED_FACE ( 'NONE', ( #12761 ), #3354, .T. ) ;
#23340=EDGE_LOOP ( 'NONE', ( #18755, #6538, #5005, #8980 ) ) ;
#23371=FACE_OUTER_BOUND ( 'NONE', #23340, .T. ) ;
#23388=CARTESIAN_POINT ( 'NONE',  ( 1.686903467613876059E-18, 14.42592346043842255, 0.000000000000000000 ) ) ;
#23422=DIRECTION ( 'NONE',  ( 0.000000000000000000, -1.000000000000000000, 0.000000000000000000 ) ) ;
#23430=EDGE_LOOP ( 'NONE', ( #8339, #22868, #14986, #20224 ) ) ;
#23534=CIRCLE ( 'NONE', #16863, 9.725923461386811297 ) ;
#23552=DIRECTION ( 'NONE',  ( 0.000000000000000000, 0.000000000000000000, 1.000000000000000000 ) ) ;
#23593=AXIS2_PLACEMENT_3D ( 'NONE', #6201, #13637, #19133 ) ;
#23610=ADVANCED_FACE ( 'NONE', ( #23271 ), #7983, .F. ) ;
#23617=ORIENTED_EDGE ( 'NONE', *, *, #17469, .T. ) ;
#23624=CARTESIAN_POINT ( 'NONE',  ( 0.000000000000000000, 0.000000000000000000, 0.000000000000000000 ) ) ;
#23684=PRODUCT ( 'Oil seal', 'Oil seal', '', ( #19968 ) ) ;
#23871=DIRECTION ( 'NONE',  ( 0.000000000000000000, 0.000000000000000000, 1.000000000000000000 ) ) ;
#23885=CIRCLE ( 'NONE', #5579, 11.24716442891539714 ) ;
#23896=EDGE_CURVE ( 'NONE', #18951, #3309, #20913, .T. ) ;
#23934=LINE ( 'NONE', #18568, #16818 ) ;
#23935=AXIS2_PLACEMENT_3D ( 'NONE', #2186, #5737, #5969 ) ;
#23970=DIRECTION ( 'NONE',  ( -1.000000000000000000, -0.000000000000000000, -0.000000000000000000 ) ) ;
#23998=DIRECTION ( 'NONE',  ( 0.000000000000000000, 0.000000000000000000, 1.000000000000000000 ) ) ;
#24041=ORIENTED_EDGE ( 'NONE', *, *, #7694, .T. ) ;
#24049=DIRECTION ( 'NONE',  ( 0.000000000000000000, 0.000000000000000000, 1.000000000000000000 ) ) ;
#24098=CARTESIAN_POINT ( 'NONE',  ( 0.000000000000000000, 0.000000000000000000, 14.72592346043842326 ) ) ;
#24156=COLOUR_RGB('Black',0.12,0.14,0.17);
#24157=FILL_AREA_STYLE_COLOUR('',#24156);
#24158=FILL_AREA_STYLE('',(#24157));
#24159=SURFACE_STYLE_FILL_AREA(#24158);
#24160=SURFACE_SIDE_STYLE('',(#24159));
#24161=SURFACE_STYLE_USAGE(.BOTH.,#24160);
#24162=PRESENTATION_STYLE_ASSIGNMENT((#24161));
ENDSEC;
END-ISO-10303-21;
